ISO-10303-21;
HEADER;
/* Generated by software containing ST-Developer
 * from STEP Tools, Inc. (www.steptools.com) 
 */

FILE_DESCRIPTION(
/* description */ ('PAT-015'),
/* implementation_level */ '2;1');

FILE_NAME(
/* name */ 'Diaphragm.step',
/* time_stamp */ '2026-10-29T16:03:43-07:00',
/* author */ (''),
/* organization */ (''),
/* preprocessor_version */ 'ST-DEVELOPER v20.2',
/* originating_system */ 'Autodesk Translation Framework v15.17.0.0',
/* authorisation */ '');

FILE_SCHEMA (('AUTOMOTIVE_DESIGN { 1 0 10303 214 3 1 1 }'));
ENDSEC;

DATA;
#10=MECHANICAL_DESIGN_GEOMETRIC_PRESENTATION_REPRESENTATION('',(#241),#10266);
#193=SHAPE_REPRESENTATION_RELATIONSHIP('SRR','None',#10364,#216);
#216=ADVANCED_BREP_SHAPE_REPRESENTATION('',(#266),#10252);
#241=STYLED_ITEM('',(#10561),#266);
#266=MANIFOLD_SOLID_BREP('Body1',#4700);
#372=FACE_BOUND('',#1095,.T.);
#373=FACE_BOUND('',#1096,.T.);
#374=FACE_BOUND('',#1097,.T.);
#375=FACE_BOUND('',#1098,.T.);
#376=FACE_BOUND('',#1099,.T.);
#377=FACE_BOUND('',#1100,.T.);
#378=FACE_BOUND('',#1101,.T.);
#379=FACE_BOUND('',#1103,.T.);
#380=FACE_BOUND('',#1104,.T.);
#381=FACE_BOUND('',#1105,.T.);
#382=FACE_BOUND('',#1106,.T.);
#383=FACE_BOUND('',#1107,.T.);
#384=FACE_BOUND('',#1108,.T.);
#385=FACE_BOUND('',#1109,.T.);
#497=PLANE('',#5287);
#498=PLANE('',#5288);
#723=FACE_OUTER_BOUND('',#1086,.T.);
#724=FACE_OUTER_BOUND('',#1087,.T.);
#725=FACE_OUTER_BOUND('',#1088,.T.);
#726=FACE_OUTER_BOUND('',#1089,.T.);
#727=FACE_OUTER_BOUND('',#1090,.T.);
#728=FACE_OUTER_BOUND('',#1091,.T.);
#729=FACE_OUTER_BOUND('',#1092,.T.);
#730=FACE_OUTER_BOUND('',#1093,.T.);
#731=FACE_OUTER_BOUND('',#1094,.T.);
#732=FACE_OUTER_BOUND('',#1102,.T.);
#1086=EDGE_LOOP('',(#3759,#3760,#3761,#3762));
#1087=EDGE_LOOP('',(#3763,#3764,#3765,#3766));
#1088=EDGE_LOOP('',(#3767,#3768,#3769,#3770));
#1089=EDGE_LOOP('',(#3771,#3772,#3773,#3774));
#1090=EDGE_LOOP('',(#3775,#3776,#3777,#3778));
#1091=EDGE_LOOP('',(#3779,#3780,#3781,#3782));
#1092=EDGE_LOOP('',(#3783,#3784,#3785,#3786));
#1093=EDGE_LOOP('',(#3787,#3788,#3789,#3790));
#1094=EDGE_LOOP('',(#3791));
#1095=EDGE_LOOP('',(#3792));
#1096=EDGE_LOOP('',(#3793));
#1097=EDGE_LOOP('',(#3794));
#1098=EDGE_LOOP('',(#3795));
#1099=EDGE_LOOP('',(#3796));
#1100=EDGE_LOOP('',(#3797));
#1101=EDGE_LOOP('',(#3798));
#1102=EDGE_LOOP('',(#3799));
#1103=EDGE_LOOP('',(#3800));
#1104=EDGE_LOOP('',(#3801));
#1105=EDGE_LOOP('',(#3802));
#1106=EDGE_LOOP('',(#3803));
#1107=EDGE_LOOP('',(#3804));
#1108=EDGE_LOOP('',(#3805));
#1109=EDGE_LOOP('',(#3806));
#1468=LINE('',#8749,#1748);
#1469=LINE('',#8755,#1749);
#1470=LINE('',#8761,#1750);
#1471=LINE('',#8767,#1751);
#1472=LINE('',#8773,#1752);
#1473=LINE('',#8779,#1753);
#1474=LINE('',#8785,#1754);
#1475=LINE('',#8791,#1755);
#1748=VECTOR('',#6291,0.275);
#1749=VECTOR('',#6298,0.275);
#1750=VECTOR('',#6305,0.275);
#1751=VECTOR('',#6312,0.275);
#1752=VECTOR('',#6319,0.275);
#1753=VECTOR('',#6326,0.275);
#1754=VECTOR('',#6333,0.16);
#1755=VECTOR('',#6340,4.);
#1999=CIRCLE('',#5264,0.275);
#2000=CIRCLE('',#5265,0.275);
#2001=CIRCLE('',#5267,0.275);
#2002=CIRCLE('',#5268,0.275);
#2003=CIRCLE('',#5270,0.275);
#2004=CIRCLE('',#5271,0.275);
#2005=CIRCLE('',#5273,0.275);
#2006=CIRCLE('',#5274,0.275);
#2007=CIRCLE('',#5276,0.275);
#2008=CIRCLE('',#5277,0.275);
#2009=CIRCLE('',#5279,0.275);
#2010=CIRCLE('',#5280,0.275);
#2011=CIRCLE('',#5282,0.16);
#2012=CIRCLE('',#5283,0.16);
#2013=CIRCLE('',#5285,4.);
#2014=CIRCLE('',#5286,4.);
#2333=VERTEX_POINT('',#8746);
#2334=VERTEX_POINT('',#8748);
#2335=VERTEX_POINT('',#8752);
#2336=VERTEX_POINT('',#8754);
#2337=VERTEX_POINT('',#8758);
#2338=VERTEX_POINT('',#8760);
#2339=VERTEX_POINT('',#8764);
#2340=VERTEX_POINT('',#8766);
#2341=VERTEX_POINT('',#8770);
#2342=VERTEX_POINT('',#8772);
#2343=VERTEX_POINT('',#8776);
#2344=VERTEX_POINT('',#8778);
#2345=VERTEX_POINT('',#8782);
#2346=VERTEX_POINT('',#8784);
#2347=VERTEX_POINT('',#8788);
#2348=VERTEX_POINT('',#8790);
#2835=EDGE_CURVE('',#2333,#2333,#1999,.T.);
#2836=EDGE_CURVE('',#2333,#2334,#1468,.T.);
#2837=EDGE_CURVE('',#2334,#2334,#2000,.T.);
#2838=EDGE_CURVE('',#2335,#2335,#2001,.T.);
#2839=EDGE_CURVE('',#2335,#2336,#1469,.T.);
#2840=EDGE_CURVE('',#2336,#2336,#2002,.T.);
#2841=EDGE_CURVE('',#2337,#2337,#2003,.T.);
#2842=EDGE_CURVE('',#2337,#2338,#1470,.T.);
#2843=EDGE_CURVE('',#2338,#2338,#2004,.T.);
#2844=EDGE_CURVE('',#2339,#2339,#2005,.T.);
#2845=EDGE_CURVE('',#2339,#2340,#1471,.T.);
#2846=EDGE_CURVE('',#2340,#2340,#2006,.T.);
#2847=EDGE_CURVE('',#2341,#2341,#2007,.T.);
#2848=EDGE_CURVE('',#2341,#2342,#1472,.T.);
#2849=EDGE_CURVE('',#2342,#2342,#2008,.T.);
#2850=EDGE_CURVE('',#2343,#2343,#2009,.T.);
#2851=EDGE_CURVE('',#2343,#2344,#1473,.T.);
#2852=EDGE_CURVE('',#2344,#2344,#2010,.T.);
#2853=EDGE_CURVE('',#2345,#2345,#2011,.T.);
#2854=EDGE_CURVE('',#2345,#2346,#1474,.T.);
#2855=EDGE_CURVE('',#2346,#2346,#2012,.T.);
#2856=EDGE_CURVE('',#2347,#2347,#2013,.T.);
#2857=EDGE_CURVE('',#2347,#2348,#1475,.T.);
#2858=EDGE_CURVE('',#2348,#2348,#2014,.T.);
#3759=ORIENTED_EDGE('',*,*,#2835,.F.);
#3760=ORIENTED_EDGE('',*,*,#2836,.T.);
#3761=ORIENTED_EDGE('',*,*,#2837,.F.);
#3762=ORIENTED_EDGE('',*,*,#2836,.F.);
#3763=ORIENTED_EDGE('',*,*,#2838,.F.);
#3764=ORIENTED_EDGE('',*,*,#2839,.T.);
#3765=ORIENTED_EDGE('',*,*,#2840,.F.);
#3766=ORIENTED_EDGE('',*,*,#2839,.F.);
#3767=ORIENTED_EDGE('',*,*,#2841,.F.);
#3768=ORIENTED_EDGE('',*,*,#2842,.T.);
#3769=ORIENTED_EDGE('',*,*,#2843,.F.);
#3770=ORIENTED_EDGE('',*,*,#2842,.F.);
#3771=ORIENTED_EDGE('',*,*,#2844,.F.);
#3772=ORIENTED_EDGE('',*,*,#2845,.T.);
#3773=ORIENTED_EDGE('',*,*,#2846,.F.);
#3774=ORIENTED_EDGE('',*,*,#2845,.F.);
#3775=ORIENTED_EDGE('',*,*,#2847,.F.);
#3776=ORIENTED_EDGE('',*,*,#2848,.T.);
#3777=ORIENTED_EDGE('',*,*,#2849,.F.);
#3778=ORIENTED_EDGE('',*,*,#2848,.F.);
#3779=ORIENTED_EDGE('',*,*,#2850,.F.);
#3780=ORIENTED_EDGE('',*,*,#2851,.T.);
#3781=ORIENTED_EDGE('',*,*,#2852,.F.);
#3782=ORIENTED_EDGE('',*,*,#2851,.F.);
#3783=ORIENTED_EDGE('',*,*,#2853,.F.);
#3784=ORIENTED_EDGE('',*,*,#2854,.T.);
#3785=ORIENTED_EDGE('',*,*,#2855,.T.);
#3786=ORIENTED_EDGE('',*,*,#2854,.F.);
#3787=ORIENTED_EDGE('',*,*,#2856,.F.);
#3788=ORIENTED_EDGE('',*,*,#2857,.T.);
#3789=ORIENTED_EDGE('',*,*,#2858,.T.);
#3790=ORIENTED_EDGE('',*,*,#2857,.F.);
#3791=ORIENTED_EDGE('',*,*,#2856,.T.);
#3792=ORIENTED_EDGE('',*,*,#2853,.T.);
#3793=ORIENTED_EDGE('',*,*,#2852,.T.);
#3794=ORIENTED_EDGE('',*,*,#2849,.T.);
#3795=ORIENTED_EDGE('',*,*,#2846,.T.);
#3796=ORIENTED_EDGE('',*,*,#2843,.T.);
#3797=ORIENTED_EDGE('',*,*,#2840,.T.);
#3798=ORIENTED_EDGE('',*,*,#2837,.T.);
#3799=ORIENTED_EDGE('',*,*,#2858,.F.);
#3800=ORIENTED_EDGE('',*,*,#2855,.F.);
#3801=ORIENTED_EDGE('',*,*,#2850,.T.);
#3802=ORIENTED_EDGE('',*,*,#2847,.T.);
#3803=ORIENTED_EDGE('',*,*,#2844,.T.);
#3804=ORIENTED_EDGE('',*,*,#2841,.T.);
#3805=ORIENTED_EDGE('',*,*,#2838,.T.);
#3806=ORIENTED_EDGE('',*,*,#2835,.T.);
#4363=CYLINDRICAL_SURFACE('',#5263,0.275);
#4364=CYLINDRICAL_SURFACE('',#5266,0.275);
#4365=CYLINDRICAL_SURFACE('',#5269,0.275);
#4366=CYLINDRICAL_SURFACE('',#5272,0.275);
#4367=CYLINDRICAL_SURFACE('',#5275,0.275);
#4368=CYLINDRICAL_SURFACE('',#5278,0.275);
#4369=CYLINDRICAL_SURFACE('',#5281,0.16);
#4370=CYLINDRICAL_SURFACE('',#5284,4.);
#4558=ADVANCED_FACE('',(#723),#4363,.F.);
#4559=ADVANCED_FACE('',(#724),#4364,.F.);
#4560=ADVANCED_FACE('',(#725),#4365,.F.);
#4561=ADVANCED_FACE('',(#726),#4366,.F.);
#4562=ADVANCED_FACE('',(#727),#4367,.F.);
#4563=ADVANCED_FACE('',(#728),#4368,.F.);
#4564=ADVANCED_FACE('',(#729),#4369,.F.);
#4565=ADVANCED_FACE('',(#730),#4370,.T.);
#4566=ADVANCED_FACE('',(#731,#372,#373,#374,#375,#376,#377,#378),#497,.T.);
#4567=ADVANCED_FACE('',(#732,#379,#380,#381,#382,#383,#384,#385),#498,.F.);
#4700=CLOSED_SHELL('',(#4558,#4559,#4560,#4561,#4562,#4563,#4564,#4565,
#4566,#4567));
#5262=AXIS2_PLACEMENT_3D('',#8744,#6285,#6286);
#5263=AXIS2_PLACEMENT_3D('',#8745,#6287,#6288);
#5264=AXIS2_PLACEMENT_3D('',#8747,#6289,#6290);
#5265=AXIS2_PLACEMENT_3D('',#8750,#6292,#6293);
#5266=AXIS2_PLACEMENT_3D('',#8751,#6294,#6295);
#5267=AXIS2_PLACEMENT_3D('',#8753,#6296,#6297);
#5268=AXIS2_PLACEMENT_3D('',#8756,#6299,#6300);
#5269=AXIS2_PLACEMENT_3D('',#8757,#6301,#6302);
#5270=AXIS2_PLACEMENT_3D('',#8759,#6303,#6304);
#5271=AXIS2_PLACEMENT_3D('',#8762,#6306,#6307);
#5272=AXIS2_PLACEMENT_3D('',#8763,#6308,#6309);
#5273=AXIS2_PLACEMENT_3D('',#8765,#6310,#6311);
#5274=AXIS2_PLACEMENT_3D('',#8768,#6313,#6314);
#5275=AXIS2_PLACEMENT_3D('',#8769,#6315,#6316);
#5276=AXIS2_PLACEMENT_3D('',#8771,#6317,#6318);
#5277=AXIS2_PLACEMENT_3D('',#8774,#6320,#6321);
#5278=AXIS2_PLACEMENT_3D('',#8775,#6322,#6323);
#5279=AXIS2_PLACEMENT_3D('',#8777,#6324,#6325);
#5280=AXIS2_PLACEMENT_3D('',#8780,#6327,#6328);
#5281=AXIS2_PLACEMENT_3D('',#8781,#6329,#6330);
#5282=AXIS2_PLACEMENT_3D('',#8783,#6331,#6332);
#5283=AXIS2_PLACEMENT_3D('',#8786,#6334,#6335);
#5284=AXIS2_PLACEMENT_3D('',#8787,#6336,#6337);
#5285=AXIS2_PLACEMENT_3D('',#8789,#6338,#6339);
#5286=AXIS2_PLACEMENT_3D('',#8792,#6341,#6342);
#5287=AXIS2_PLACEMENT_3D('',#8793,#6343,#6344);
#5288=AXIS2_PLACEMENT_3D('',#8794,#6345,#6346);
#6285=DIRECTION('axis',(0.,0.,1.));
#6286=DIRECTION('refdir',(1.,0.,0.));
#6287=DIRECTION('center_axis',(0.,0.,1.));
#6288=DIRECTION('ref_axis',(1.,0.,0.));
#6289=DIRECTION('center_axis',(0.,0.,1.));
#6290=DIRECTION('ref_axis',(1.,0.,0.));
#6291=DIRECTION('',(0.,0.,1.));
#6292=DIRECTION('center_axis',(0.,0.,-1.));
#6293=DIRECTION('ref_axis',(1.,0.,0.));
#6294=DIRECTION('center_axis',(0.,0.,1.));
#6295=DIRECTION('ref_axis',(1.,0.,0.));
#6296=DIRECTION('center_axis',(0.,0.,1.));
#6297=DIRECTION('ref_axis',(1.,0.,0.));
#6298=DIRECTION('',(0.,0.,1.));
#6299=DIRECTION('center_axis',(0.,0.,-1.));
#6300=DIRECTION('ref_axis',(1.,0.,0.));
#6301=DIRECTION('center_axis',(0.,0.,1.));
#6302=DIRECTION('ref_axis',(1.,0.,0.));
#6303=DIRECTION('center_axis',(0.,0.,1.));
#6304=DIRECTION('ref_axis',(1.,0.,0.));
#6305=DIRECTION('',(0.,0.,1.));
#6306=DIRECTION('center_axis',(0.,0.,-1.));
#6307=DIRECTION('ref_axis',(1.,0.,0.));
#6308=DIRECTION('center_axis',(0.,0.,1.));
#6309=DIRECTION('ref_axis',(1.,0.,0.));
#6310=DIRECTION('center_axis',(0.,0.,1.));
#6311=DIRECTION('ref_axis',(1.,0.,0.));
#6312=DIRECTION('',(0.,0.,1.));
#6313=DIRECTION('center_axis',(0.,0.,-1.));
#6314=DIRECTION('ref_axis',(1.,0.,0.));
#6315=DIRECTION('center_axis',(0.,0.,1.));
#6316=DIRECTION('ref_axis',(1.,0.,0.));
#6317=DIRECTION('center_axis',(0.,0.,1.));
#6318=DIRECTION('ref_axis',(1.,0.,0.));
#6319=DIRECTION('',(0.,0.,1.));
#6320=DIRECTION('center_axis',(0.,0.,-1.));
#6321=DIRECTION('ref_axis',(1.,0.,0.));
#6322=DIRECTION('center_axis',(0.,0.,1.));
#6323=DIRECTION('ref_axis',(1.,0.,0.));
#6324=DIRECTION('center_axis',(0.,0.,1.));
#6325=DIRECTION('ref_axis',(1.,0.,0.));
#6326=DIRECTION('',(0.,0.,1.));
#6327=DIRECTION('center_axis',(0.,0.,-1.));
#6328=DIRECTION('ref_axis',(1.,0.,0.));
#6329=DIRECTION('center_axis',(0.,0.,1.));
#6330=DIRECTION('ref_axis',(1.,0.,0.));
#6331=DIRECTION('center_axis',(0.,0.,-1.));
#6332=DIRECTION('ref_axis',(1.,0.,0.));
#6333=DIRECTION('',(0.,0.,-1.));
#6334=DIRECTION('center_axis',(0.,0.,-1.));
#6335=DIRECTION('ref_axis',(1.,0.,0.));
#6336=DIRECTION('center_axis',(0.,0.,1.));
#6337=DIRECTION('ref_axis',(1.,0.,0.));
#6338=DIRECTION('center_axis',(0.,0.,1.));
#6339=DIRECTION('ref_axis',(1.,0.,0.));
#6340=DIRECTION('',(0.,0.,-1.));
#6341=DIRECTION('center_axis',(0.,0.,1.));
#6342=DIRECTION('ref_axis',(1.,0.,0.));
#6343=DIRECTION('center_axis',(0.,0.,1.));
#6344=DIRECTION('ref_axis',(1.,0.,0.));
#6345=DIRECTION('center_axis',(0.,0.,1.));
#6346=DIRECTION('ref_axis',(1.,0.,0.));
#8744=CARTESIAN_POINT('',(0.,0.,0.));
#8745=CARTESIAN_POINT('Origin',(-6.2456986756515E-16,-3.4,4.9));
#8746=CARTESIAN_POINT('',(-0.275000000000001,-3.4,5.));
#8747=CARTESIAN_POINT('Origin',(-6.2456986756515E-16,-3.4,5.));
#8748=CARTESIAN_POINT('',(-0.275000000000001,-3.4,5.1));
#8749=CARTESIAN_POINT('',(-0.275000000000001,-3.4,4.9));
#8750=CARTESIAN_POINT('Origin',(-6.2456986756515E-16,-3.4,5.1));
#8751=CARTESIAN_POINT('Origin',(2.94448637286709,1.7,4.9));
#8752=CARTESIAN_POINT('',(2.66948637286709,1.7,5.));
#8753=CARTESIAN_POINT('Origin',(2.94448637286709,1.7,5.));
#8754=CARTESIAN_POINT('',(2.66948637286709,1.7,5.1));
#8755=CARTESIAN_POINT('',(2.66948637286709,1.7,4.9));
#8756=CARTESIAN_POINT('Origin',(2.94448637286709,1.7,5.1));
#8757=CARTESIAN_POINT('Origin',(2.0818995585505E-16,3.4,4.9));
#8758=CARTESIAN_POINT('',(-0.275,3.4,5.));
#8759=CARTESIAN_POINT('Origin',(2.0818995585505E-16,3.4,5.));
#8760=CARTESIAN_POINT('',(-0.275,3.4,5.1));
#8761=CARTESIAN_POINT('',(-0.275,3.4,4.9));
#8762=CARTESIAN_POINT('Origin',(2.0818995585505E-16,3.4,5.1));
#8763=CARTESIAN_POINT('Origin',(-2.94448637286709,1.7,4.9));
#8764=CARTESIAN_POINT('',(-3.21948637286709,1.7,5.));
#8765=CARTESIAN_POINT('Origin',(-2.94448637286709,1.7,5.));
#8766=CARTESIAN_POINT('',(-3.21948637286709,1.7,5.1));
#8767=CARTESIAN_POINT('',(-3.21948637286709,1.7,4.9));
#8768=CARTESIAN_POINT('Origin',(-2.94448637286709,1.7,5.1));
#8769=CARTESIAN_POINT('Origin',(-2.94448637286709,-1.7,4.9));
#8770=CARTESIAN_POINT('',(-3.21948637286709,-1.7,5.));
#8771=CARTESIAN_POINT('Origin',(-2.94448637286709,-1.7,5.));
#8772=CARTESIAN_POINT('',(-3.21948637286709,-1.7,5.1));
#8773=CARTESIAN_POINT('',(-3.21948637286709,-1.7,4.9));
#8774=CARTESIAN_POINT('Origin',(-2.94448637286709,-1.7,5.1));
#8775=CARTESIAN_POINT('Origin',(2.94448637286709,-1.7,4.9));
#8776=CARTESIAN_POINT('',(2.66948637286709,-1.7,5.));
#8777=CARTESIAN_POINT('Origin',(2.94448637286709,-1.7,5.));
#8778=CARTESIAN_POINT('',(2.66948637286709,-1.7,5.1));
#8779=CARTESIAN_POINT('',(2.66948637286709,-1.7,4.9));
#8780=CARTESIAN_POINT('Origin',(2.94448637286709,-1.7,5.1));
#8781=CARTESIAN_POINT('Origin',(0.,0.,5.));
#8782=CARTESIAN_POINT('',(-0.16,-1.95943487863577E-17,5.1));
#8783=CARTESIAN_POINT('Origin',(0.,0.,5.1));
#8784=CARTESIAN_POINT('',(-0.16,-1.95943487863577E-17,5.));
#8785=CARTESIAN_POINT('',(-0.16,-1.95943487863577E-17,5.));
#8786=CARTESIAN_POINT('Origin',(0.,0.,5.));
#8787=CARTESIAN_POINT('Origin',(0.,0.,5.));
#8788=CARTESIAN_POINT('',(-4.,-4.89858719658941E-16,5.1));
#8789=CARTESIAN_POINT('Origin',(0.,0.,5.1));
#8790=CARTESIAN_POINT('',(-4.,-4.89858719658941E-16,5.));
#8791=CARTESIAN_POINT('',(-4.,-4.89858719658941E-16,5.));
#8792=CARTESIAN_POINT('Origin',(0.,0.,5.));
#8793=CARTESIAN_POINT('Origin',(0.,0.,5.1));
#8794=CARTESIAN_POINT('Origin',(0.,0.,5.));
#10227=UNCERTAINTY_MEASURE_WITH_UNIT(LENGTH_MEASURE(0.001),#10267,
'DISTANCE_ACCURACY_VALUE',
'Maximum model space distance between geometric entities at asserted c
onnectivities');
#10241=UNCERTAINTY_MEASURE_WITH_UNIT(LENGTH_MEASURE(0.001),#10267,
'DISTANCE_ACCURACY_VALUE',
'Maximum model space distance between geometric entities at asserted c
onnectivities');
#10252=(
GEOMETRIC_REPRESENTATION_CONTEXT(3)
GLOBAL_UNCERTAINTY_ASSIGNED_CONTEXT((#10227))
GLOBAL_UNIT_ASSIGNED_CONTEXT((#10267,#10269,#10270))
REPRESENTATION_CONTEXT('','3D')
);
#10266=(
GEOMETRIC_REPRESENTATION_CONTEXT(3)
GLOBAL_UNCERTAINTY_ASSIGNED_CONTEXT((#10241))
GLOBAL_UNIT_ASSIGNED_CONTEXT((#10267,#10269,#10270))
REPRESENTATION_CONTEXT('','3D')
);
#10267=(
LENGTH_UNIT()
NAMED_UNIT(*)
SI_UNIT(.CENTI.,.METRE.)
);
#10269=(
NAMED_UNIT(*)
PLANE_ANGLE_UNIT()
SI_UNIT($,.RADIAN.)
);
#10270=(
NAMED_UNIT(*)
SI_UNIT($,.STERADIAN.)
SOLID_ANGLE_UNIT()
);
#10281=SHAPE_DEFINITION_REPRESENTATION(#10305,#10364);
#10305=PRODUCT_DEFINITION_SHAPE('',$,#10389);
#10364=SHAPE_REPRESENTATION('',(#5262),#10252);
#10378=PRODUCT_DEFINITION_CONTEXT('part definition',#10452,'design');
#10389=PRODUCT_DEFINITION('Diaphragm','Diaphragm',#10413,
#10378);
#10413=PRODUCT_DEFINITION_FORMATION('',$,#10464);
#10452=APPLICATION_CONTEXT(
'Core Data for Automotive Mechanical Design Process');
#10453=PRODUCT_CONTEXT('part definition',#10452,'mechanical');
#10464=PRODUCT('Diaphragm','Diaphragm','Diaphragm',(#10453));
#10555=COLOUR_RGB('Off White',0.89,0.88,0.83);
#10556=FILL_AREA_STYLE_COLOUR('',#10555);
#10557=FILL_AREA_STYLE('',(#10556));
#10558=SURFACE_STYLE_FILL_AREA(#10557);
#10559=SURFACE_SIDE_STYLE('',(#10558));
#10560=SURFACE_STYLE_USAGE(.BOTH.,#10559);
#10561=PRESENTATION_STYLE_ASSIGNMENT((#10560));
ENDSEC;
END-ISO-10303-21;
